ISO-10303-21;
HEADER;
/* Generated by software containing ST-Developer
 * from STEP Tools, Inc. (www.steptools.com) 
 */

FILE_DESCRIPTION(
/* description */ (''),
/* implementation_level */ '2;1');

FILE_NAME(
/* name */ '02_Neodymium_Disc_Magnet_N35_10x2.step',
/* time_stamp */ '2026-10-11T08:53:36-07:00',
/* author */ (''),
/* organization */ (''),
/* preprocessor_version */ 'ST-DEVELOPER v20.2',
/* originating_system */ 'Autodesk Translation Framework v15.15.0.0',
/* authorisation */ '');

FILE_SCHEMA (('AUTOMOTIVE_DESIGN { 1 0 10303 214 3 1 1 }'));
ENDSEC;

DATA;
#10=MECHANICAL_DESIGN_GEOMETRIC_PRESENTATION_REPRESENTATION('',(#73),#3338);
#65=SHAPE_REPRESENTATION_RELATIONSHIP('SRR','None',#3368,#69);
#69=ADVANCED_BREP_SHAPE_REPRESENTATION('',(#77),#3335);
#73=STYLED_ITEM('',(#3450),#77);
#77=MANIFOLD_SOLID_BREP('Body1',#1575);
#137=CYLINDRICAL_SURFACE('',#1786,5.);
#187=PLANE('',#1788);
#188=PLANE('',#1791);
#272=FACE_OUTER_BOUND('',#394,.T.);
#273=FACE_OUTER_BOUND('',#395,.T.);
#274=FACE_OUTER_BOUND('',#396,.T.);
#275=FACE_OUTER_BOUND('',#397,.T.);
#276=FACE_OUTER_BOUND('',#398,.T.);
#394=EDGE_LOOP('',(#1414,#1415,#1416,#1417));
#395=EDGE_LOOP('',(#1418,#1419,#1420,#1421));
#396=EDGE_LOOP('',(#1422));
#397=EDGE_LOOP('',(#1423,#1424,#1425,#1426));
#398=EDGE_LOOP('',(#1427));
#496=LINE('',#3280,#593);
#497=LINE('',#3285,#594);
#498=LINE('',#3290,#595);
#593=VECTOR('',#2233,4.9);
#594=VECTOR('',#2240,5.);
#595=VECTOR('',#2247,4.9);
#675=CIRCLE('',#1784,5.);
#676=CIRCLE('',#1785,4.8);
#677=CIRCLE('',#1787,5.);
#678=CIRCLE('',#1790,4.8);
#804=VERTEX_POINT('',#3277);
#805=VERTEX_POINT('',#3279);
#806=VERTEX_POINT('',#3283);
#807=VERTEX_POINT('',#3288);
#1009=EDGE_CURVE('',#804,#804,#675,.T.);
#1010=EDGE_CURVE('',#804,#805,#496,.T.);
#1011=EDGE_CURVE('',#805,#805,#676,.T.);
#1012=EDGE_CURVE('',#806,#806,#677,.T.);
#1013=EDGE_CURVE('',#806,#804,#497,.T.);
#1014=EDGE_CURVE('',#807,#807,#678,.T.);
#1015=EDGE_CURVE('',#807,#806,#498,.T.);
#1414=ORIENTED_EDGE('',*,*,#1009,.T.);
#1415=ORIENTED_EDGE('',*,*,#1010,.T.);
#1416=ORIENTED_EDGE('',*,*,#1011,.T.);
#1417=ORIENTED_EDGE('',*,*,#1010,.F.);
#1418=ORIENTED_EDGE('',*,*,#1012,.F.);
#1419=ORIENTED_EDGE('',*,*,#1013,.T.);
#1420=ORIENTED_EDGE('',*,*,#1009,.F.);
#1421=ORIENTED_EDGE('',*,*,#1013,.F.);
#1422=ORIENTED_EDGE('',*,*,#1011,.F.);
#1423=ORIENTED_EDGE('',*,*,#1014,.T.);
#1424=ORIENTED_EDGE('',*,*,#1015,.T.);
#1425=ORIENTED_EDGE('',*,*,#1012,.T.);
#1426=ORIENTED_EDGE('',*,*,#1015,.F.);
#1427=ORIENTED_EDGE('',*,*,#1014,.F.);
#1478=CONICAL_SURFACE('',#1783,4.9,0.785398163397449);
#1479=CONICAL_SURFACE('',#1789,4.9,0.785398163397448);
#1563=ADVANCED_FACE('',(#272),#1478,.T.);
#1564=ADVANCED_FACE('',(#273),#137,.T.);
#1565=ADVANCED_FACE('',(#274),#187,.F.);
#1566=ADVANCED_FACE('',(#275),#1479,.T.);
#1567=ADVANCED_FACE('',(#276),#188,.T.);
#1575=CLOSED_SHELL('',(#1563,#1564,#1565,#1566,#1567));
#1782=AXIS2_PLACEMENT_3D('',#3275,#2227,#2228);
#1783=AXIS2_PLACEMENT_3D('',#3276,#2229,#2230);
#1784=AXIS2_PLACEMENT_3D('',#3278,#2231,#2232);
#1785=AXIS2_PLACEMENT_3D('',#3281,#2234,#2235);
#1786=AXIS2_PLACEMENT_3D('',#3282,#2236,#2237);
#1787=AXIS2_PLACEMENT_3D('',#3284,#2238,#2239);
#1788=AXIS2_PLACEMENT_3D('',#3286,#2241,#2242);
#1789=AXIS2_PLACEMENT_3D('',#3287,#2243,#2244);
#1790=AXIS2_PLACEMENT_3D('',#3289,#2245,#2246);
#1791=AXIS2_PLACEMENT_3D('',#3291,#2248,#2249);
#2227=DIRECTION('axis',(0.,0.,1.));
#2228=DIRECTION('refdir',(1.,0.,0.));
#2229=DIRECTION('center_axis',(0.,0.,1.));
#2230=DIRECTION('ref_axis',(1.,0.,0.));
#2231=DIRECTION('center_axis',(0.,0.,-1.));
#2232=DIRECTION('ref_axis',(1.,0.,0.));
#2233=DIRECTION('',(0.707106781186548,8.65956056235494E-17,-0.707106781186547));
#2234=DIRECTION('center_axis',(0.,0.,1.));
#2235=DIRECTION('ref_axis',(1.,0.,0.));
#2236=DIRECTION('center_axis',(0.,0.,1.));
#2237=DIRECTION('ref_axis',(1.,0.,0.));
#2238=DIRECTION('center_axis',(0.,0.,1.));
#2239=DIRECTION('ref_axis',(1.,0.,0.));
#2240=DIRECTION('',(0.,0.,-1.));
#2241=DIRECTION('center_axis',(0.,0.,1.));
#2242=DIRECTION('ref_axis',(1.,0.,0.));
#2243=DIRECTION('center_axis',(0.,0.,-1.));
#2244=DIRECTION('ref_axis',(1.,0.,0.));
#2245=DIRECTION('center_axis',(0.,0.,-1.));
#2246=DIRECTION('ref_axis',(1.,0.,0.));
#2247=DIRECTION('',(-0.707106781186548,-8.65956056235494E-17,-0.707106781186548));
#2248=DIRECTION('center_axis',(0.,0.,1.));
#2249=DIRECTION('ref_axis',(1.,0.,0.));
#3275=CARTESIAN_POINT('',(0.,0.,0.));
#3276=CARTESIAN_POINT('Origin',(0.,0.,0.1));
#3277=CARTESIAN_POINT('',(-5.,6.12323399573677E-16,0.2));
#3278=CARTESIAN_POINT('Origin',(0.,0.,0.2));
#3279=CARTESIAN_POINT('',(-4.8,-5.87830463590729E-16,0.));
#3280=CARTESIAN_POINT('',(-4.9,-6.00076931582203E-16,0.1));
#3281=CARTESIAN_POINT('Origin',(0.,0.,0.));
#3282=CARTESIAN_POINT('Origin',(0.,0.,0.));
#3283=CARTESIAN_POINT('',(-5.,-6.12323399573677E-16,1.8));
#3284=CARTESIAN_POINT('Origin',(0.,0.,1.8));
#3285=CARTESIAN_POINT('',(-5.,-6.12323399573677E-16,0.));
#3286=CARTESIAN_POINT('Origin',(0.,0.,0.));
#3287=CARTESIAN_POINT('Origin',(0.,0.,1.9));
#3288=CARTESIAN_POINT('',(-4.8,5.87830463590729E-16,2.));
#3289=CARTESIAN_POINT('Origin',(0.,0.,2.));
#3290=CARTESIAN_POINT('',(-4.9,-6.00076931582203E-16,1.9));
#3291=CARTESIAN_POINT('Origin',(0.,0.,2.));
#3329=UNCERTAINTY_MEASURE_WITH_UNIT(LENGTH_MEASURE(0.01),#3339,
'DISTANCE_ACCURACY_VALUE',
'Maximum model space distance between geometric entities at asserted c
onnectivities');
#3332=UNCERTAINTY_MEASURE_WITH_UNIT(LENGTH_MEASURE(0.01),#3339,
'DISTANCE_ACCURACY_VALUE',
'Maximum model space distance between geometric entities at asserted c
onnectivities');
#3335=(
GEOMETRIC_REPRESENTATION_CONTEXT(3)
GLOBAL_UNCERTAINTY_ASSIGNED_CONTEXT((#3329))
GLOBAL_UNIT_ASSIGNED_CONTEXT((#3339,#3341,#3342))
REPRESENTATION_CONTEXT('','3D')
);
#3338=(
GEOMETRIC_REPRESENTATION_CONTEXT(3)
GLOBAL_UNCERTAINTY_ASSIGNED_CONTEXT((#3332))
GLOBAL_UNIT_ASSIGNED_CONTEXT((#3339,#3341,#3342))
REPRESENTATION_CONTEXT('','3D')
);
#3339=(
LENGTH_UNIT()
NAMED_UNIT(*)
SI_UNIT(.MILLI.,.METRE.)
);
#3341=(
NAMED_UNIT(*)
PLANE_ANGLE_UNIT()
SI_UNIT($,.RADIAN.)
);
#3342=(
NAMED_UNIT(*)
SI_UNIT($,.STERADIAN.)
SOLID_ANGLE_UNIT()
);
#3345=SHAPE_DEFINITION_REPRESENTATION(#3350,#3368);
#3350=PRODUCT_DEFINITION_SHAPE('',$,#3374);
#3368=SHAPE_REPRESENTATION('',(#1782),#3335);
#3371=PRODUCT_DEFINITION_CONTEXT('part definition',#3388,'design');
#3374=PRODUCT_DEFINITION('2026-10-11-08-53-16-563',
'02_Neodymium_Disc_Magnet_N35_10x2',#3379,#3371);
#3379=PRODUCT_DEFINITION_FORMATION('',$,#3392);
#3388=APPLICATION_CONTEXT(
'Core Data for Automotive Mechanical Design Process');
#3389=PRODUCT_CONTEXT('part definition',#3388,'mechanical');
#3392=PRODUCT('2026-10-11-08-53-16-563',
'02_Neodymium_Disc_Magnet_N35_10x2',$,(#3389));
#3444=COLOUR_RGB('Sky Blue',0.24,0.69,0.87);
#3445=FILL_AREA_STYLE_COLOUR('',#3444);
#3446=FILL_AREA_STYLE('',(#3445));
#3447=SURFACE_STYLE_FILL_AREA(#3446);
#3448=SURFACE_SIDE_STYLE('',(#3447));
#3449=SURFACE_STYLE_USAGE(.BOTH.,#3448);
#3450=PRESENTATION_STYLE_ASSIGNMENT((#3449));
ENDSEC;
END-ISO-10303-21;
